ISO-10303-21;
HEADER;
FILE_DESCRIPTION (('STEP AP214'),
    '1' );
FILE_NAME ('Boring Bar Holder.step',
    '2026-10-09T18:50:44',
    ( '' ),
    ( '' ),
    'SwSTEP 2.0',
    'SolidWorks 2026',
    '' );
FILE_SCHEMA (( 'AUTOMOTIVE_DESIGN' ));
ENDSEC;

DATA;
#22=CARTESIAN_POINT ( 'NONE',  ( -15.49969986081095996, -67.00737899243799234, -5.497689735156000346 ) ) ;
#40=CARTESIAN_POINT ( 'NONE',  ( -10.66443468489866220, -90.61811337294874136, -7.838004541461820907 ) ) ;
#60=CARTESIAN_POINT ( 'NONE',  ( -15.49969986081091555, -109.7266455319748957, -5.512402352389309534 ) ) ;
#76=ADVANCED_BREP_SHAPE_REPRESENTATION ( '', ( #2616, #6789 ), #5587 ) ;
#98=CARTESIAN_POINT ( 'NONE',  ( -20.86490974387957209, -107.8289007898295182, -5.225852060212539563 ) ) ;
#160=CARTESIAN_POINT ( 'NONE',  ( -20.87112600995946110, -106.2635794615412834, -5.497689735156005675 ) ) ;
#228=LINE ( 'NONE', #8628, #3240 ) ;
#250=CYLINDRICAL_SURFACE ( 'NONE', #2706, 6.000000000000000000 ) ;
#264=PRODUCT ( 'Boring Bar Holder', 'Boring Bar Holder', '', ( #2047 ) ) ;
#269=CARTESIAN_POINT ( 'NONE',  ( -11.86438417805047862, -90.99861266563027584, -9.452020815084084759 ) ) ;
#302=EDGE_CURVE ( 'NONE', #14153, #6582, #13638, .T. ) ;
#303=EDGE_CURVE ( 'NONE', #11878, #6778, #8167, .T. ) ;
#328=PLANE ( 'NONE',  #5014 ) ;
#352=CONICAL_SURFACE ( 'NONE', #10852, 6.000000000000001776, 0.03490658503988566114 ) ;
#434=CIRCLE ( 'NONE', #12892, 6.000000000000001776 ) ;
#447=SURFACE_SIDE_STYLE ('',( #4964 ) ) ;
#481=AXIS2_PLACEMENT_3D ( 'NONE', #6278, #6351, #14474 ) ;
#534=DIRECTION ( 'NONE',  ( -1.000000000000000078E-15, 1.000000000000000000, 0.000000000000000000 ) ) ;
#583=CARTESIAN_POINT ( 'NONE',  ( -20.87112600995946465, -106.1573670789699406, -5.659460905592496260 ) ) ;
#607=CARTESIAN_POINT ( 'NONE',  ( -16.09969986081092941, -93.78236537426951713, -11.11889594355865185 ) ) ;
#644=FACE_OUTER_BOUND ( 'NONE', #1193, .T. ) ;
#690=DIRECTION ( 'NONE',  ( -1.000000000000000000, -1.000000000000000078E-15, -1.000000000000000078E-15 ) ) ;
#746=CARTESIAN_POINT ( 'NONE',  ( -100.5053766806731090, -107.1622034095863825, -5.012689735156086179 ) ) ;
#749=EDGE_CURVE ( 'NONE', #5139, #2245, #3034, .T. ) ;
#752=B_SPLINE_CURVE_WITH_KNOTS ( 'NONE', 3,
 ( #2088, #3384, #15008, #9112, #3309, #13862, #14858, #6728 ),
 .UNSPECIFIED., .F., .F.,
 ( 4, 2, 2, 4 ),
 ( 0.003401025496237318393, 0.003933919667760182350, 0.004200366753521614545, 0.004466813839283045873 ),
 .UNSPECIFIED. ) ;
#803=ORIENTED_EDGE ( 'NONE', *, *, #14109, .T. ) ;
#811=FACE_OUTER_BOUND ( 'NONE', #5285, .T. ) ;
#880=ADVANCED_FACE ( 'NONE', ( #811 ), #352, .T. ) ;
#933=ORIENTED_EDGE ( 'NONE', *, *, #6988, .F. ) ;
#942=EDGE_CURVE ( 'NONE', #1308, #14720, #2548, .T. ) ;
#959=CARTESIAN_POINT ( 'NONE',  ( -10.59914214906130780, -90.60588013820681397, -7.696961324692049189 ) ) ;
#971=CARTESIAN_POINT ( 'NONE',  ( -18.64620844969664759, -109.4443699603185678, -0.1262635860074659000 ) ) ;
#974=ORIENTED_EDGE ( 'NONE', *, *, #1401, .T. ) ;
#984=CARTESIAN_POINT ( 'NONE',  ( -10.29813411369431719, -90.56073884152880282, -4.157226901606094316 ) ) ;
#1006=ORIENTED_EDGE ( 'NONE', *, *, #10301, .T. ) ;
#1054=DIRECTION ( 'NONE',  ( -1.050965490997517593E-15, 0.05233595624294359872, 0.9986295347545739443 ) ) ;
#1101=EDGE_CURVE ( 'NONE', #6582, #14153, #10860, .T. ) ;
#1103=CARTESIAN_POINT ( 'NONE',  ( -10.12676381431746542, -90.53940471697117687, -5.497640657892870486 ) ) ;
#1125=CARTESIAN_POINT ( 'NONE',  ( -27.99969986081091733, -109.7258744763782943, -5.497689735156013668 ) ) ;
#1127=CARTESIAN_POINT ( 'NONE',  ( -18.09969986081091875, -107.1622034095862972, -6.087689735156002868 ) ) ;
#1140=CARTESIAN_POINT ( 'NONE',  ( -20.62495262810510610, -107.5503273669732067, -7.108481602779681552 ) ) ;
#1178=CARTESIAN_POINT ( 'NONE',  ( -18.09969986081091520, -109.8057294739168981, -7.021413858388623197 ) ) ;
#1179=CARTESIAN_POINT ( 'NONE',  ( -11.06942950089595712, -90.71429950798489017, -8.540436891703901523 ) ) ;
#1180=DIRECTION ( 'NONE',  ( 1.000000000000000078E-15, -1.000000000000000000, 0.000000000000000000 ) ) ;
#1193=EDGE_LOOP ( 'NONE', ( #4642, #14603, #14008, #14703 ) ) ;
#1235=DIRECTION ( 'NONE',  ( 1.000000000000000000, 0.000000000000000000, 1.011922027653137537E-15 ) ) ;
#1238=CARTESIAN_POINT ( 'NONE',  ( -20.87112600995948242, -85.00737899243800655, -5.497689735156005675 ) ) ;
#1252=CARTESIAN_POINT ( 'NONE',  ( -14.49553980497220174, -93.09698010465587004, -10.78611153367636888 ) ) ;
#1308=VERTEX_POINT ( 'NONE', #8943 ) ;
#1336=CARTESIAN_POINT ( 'NONE',  ( -11.85919799147835363, -90.99634588947422742, -9.447245264708476142 ) ) ;
#1399=AXIS2_PLACEMENT_3D ( 'NONE', #1868, #13648, #1714 ) ;
#1401=EDGE_CURVE ( 'NONE', #10974, #3638, #5757, .T. ) ;
#1422=ORIENTED_EDGE ( 'NONE', *, *, #7827, .T. ) ;
#1486=CARTESIAN_POINT ( 'NONE',  ( -12.20995213488984277, -91.16154615634617642, -9.744773464311498046 ) ) ;
#1509=CARTESIAN_POINT ( 'NONE',  ( -15.49969986081095996, -67.00737899243799234, -5.497689735156000346 ) ) ;
#1514=ORIENTED_EDGE ( 'NONE', *, *, #942, .T. ) ;
#1543=SHAPE_DEFINITION_REPRESENTATION ( #9665, #2852 ) ;
#1555=CARTESIAN_POINT ( 'NONE',  ( -14.84437367148764686, -93.78075803281299727, -10.82899037021154953 ) ) ;
#1591=ADVANCED_FACE ( 'NONE', ( #4273 ), #3045, .T. ) ;
#1636=ORIENTED_EDGE ( 'NONE', *, *, #3326, .F. ) ;
#1637=DIRECTION ( 'NONE',  ( 1.000000000000000000, 1.000000000000000078E-15, 1.000000000000000078E-15 ) ) ;
#1649=( BOUNDED_CURVE ( )  B_SPLINE_CURVE ( 3, ( #2084, #6806, #7878, #11263 ),
 .UNSPECIFIED., .F., .T. ) 
 B_SPLINE_CURVE_WITH_KNOTS ( ( 4, 4 ),
 ( 3.646861569849260576, 4.712388980384689674 ),
 .UNSPECIFIED. ) 
 CURVE ( )  GEOMETRIC_REPRESENTATION_ITEM ( )  RATIONAL_B_SPLINE_CURVE ( ( 1.000000000000000000, 0.9076044213655485304, 0.9076044213655485304, 1.000000000000000000 ) ) 
 REPRESENTATION_ITEM ( '' )  );
#1668=AXIS2_PLACEMENT_3D ( 'NONE', #14800, #2333, #11359 ) ;
#1687=DIRECTION ( 'NONE',  ( -0.9757243316563987134, -0.01146169732403567489, -0.2187022133132769386 ) ) ;
#1714=DIRECTION ( 'NONE',  ( -1.000000000000000000, 0.000000000000000000, -1.011922027653137143E-15 ) ) ;
#1720=EDGE_CURVE ( 'NONE', #14153, #8778, #13833, .T. ) ;
#1725=CARTESIAN_POINT ( 'NONE',  ( -15.49969986081095996, -67.00737899243799234, -5.497689735156000346 ) ) ;
#1728=DIRECTION ( 'NONE',  ( -1.000000000000000000, -1.000000000000000078E-15, -1.000000000000000078E-15 ) ) ;
#1867=CARTESIAN_POINT ( 'NONE',  ( -15.49969986081091555, -110.0073789924380065, -5.497689735155995017 ) ) ;
#1868=CARTESIAN_POINT ( 'NONE',  ( -15.49969986081095996, -67.00737899243799234, -5.497689735156000346 ) ) ;
#1902=EDGE_LOOP ( 'NONE', ( #9229, #10233 ) ) ;
#1989=CARTESIAN_POINT ( 'NONE',  ( -15.49969986081099904, -27.00737899243799944, -5.497689735156000346 ) ) ;
#2017=VERTEX_POINT ( 'NONE', #8215 ) ;
#2030=EDGE_CURVE ( 'NONE', #2942, #6582, #7059, .T. ) ;
#2042=CARTESIAN_POINT ( 'NONE',  ( -100.5053766806731090, -107.1622034095863825, -6.087689735156085469 ) ) ;
#2047=PRODUCT_CONTEXT ( 'NONE', #9961, 'mechanical' ) ;
#2054=CARTESIAN_POINT ( 'NONE',  ( -15.18865579839852487, -94.57871019452736050, -0.1345408968949149964 ) ) ;
#2064=AXIS2_PLACEMENT_3D ( 'NONE', #9708, #13386, #10930 ) ;
#2084=CARTESIAN_POINT ( 'NONE',  ( -18.09969986081091164, -109.9722034095862995, -10.19792577984107318 ) ) ;
#2088=CARTESIAN_POINT ( 'NONE',  ( -20.84918524500973191, -107.1622034095862972, -5.012689735156006243 ) ) ;
#2127=DIRECTION ( 'NONE',  ( -1.000000000000000000, -1.000000000000000078E-15, -1.000000000000000078E-15 ) ) ;
#2133=VECTOR ( 'NONE', #2205, 1000.000000000000000 ) ;
#2155=FILL_AREA_STYLE_COLOUR ( '', #11648 ) ;
#2175=VERTEX_POINT ( 'NONE', #7369 ) ;
#2189=ORIENTED_EDGE ( 'NONE', *, *, #13571, .F. ) ;
#2204=CARTESIAN_POINT ( 'NONE',  ( -14.81665476263932213, -93.72685551323446873, -0.1697857866622040635 ) ) ;
#2205=DIRECTION ( 'NONE',  ( 0.03489949670249904018, 0.9993908270190957621, 3.917345239535707520E-17 ) ) ;
#2245=VERTEX_POINT ( 'NONE', #6444 ) ;
#2271=DIRECTION ( 'NONE',  ( 0.000000000000000000, 0.000000000000000000, -1.000000000000000000 ) ) ;
#2288=VERTEX_POINT ( 'NONE', #6296 ) ;
#2292=CARTESIAN_POINT ( 'NONE',  ( -15.49969986081094042, -85.00737899243800655, -5.497689735156000346 ) ) ;
#2333=DIRECTION ( 'NONE',  ( 1.000000000000000078E-15, -1.000000000000000000, 0.000000000000000000 ) ) ;
#2343=ADVANCED_FACE ( 'NONE', ( #644 ), #8225, .T. ) ;
#2359=CARTESIAN_POINT ( 'NONE',  ( -10.12827607185207235, -90.53858270881919168, -5.246309576803675156 ) ) ;
#2368=DIRECTION ( 'NONE',  ( -1.000000000000000078E-15, 1.000000000000000000, 0.000000000000000000 ) ) ;
#2392=FACE_OUTER_BOUND ( 'NONE', #5590, .T. ) ;
#2410=CARTESIAN_POINT ( 'NONE',  ( -11.87316907169401148, -91.00246572745722062, -9.460079019236541598 ) ) ;
#2472=ORIENTED_EDGE ( 'NONE', *, *, #302, .F. ) ;
#2481=DIRECTION ( 'NONE',  ( 1.000000000000000078E-15, -1.000000000000000000, 0.000000000000000000 ) ) ;
#2500=AXIS2_PLACEMENT_3D ( 'NONE', #2042, #12603, #2271 ) ;
#2524=CARTESIAN_POINT ( 'NONE',  ( -20.79197367102019456, -108.1981419463315319, -6.432195627249867265 ) ) ;
#2533=AXIS2_PLACEMENT_3D ( 'NONE', #8858, #534, #13538 ) ;
#2548=CIRCLE ( 'NONE', #11095, 6.000000000000000000 ) ;
#2559=CARTESIAN_POINT ( 'NONE',  ( -12.42399349929057095, -91.27394999476267401, -9.904958159143182783 ) ) ;
#2612=CARTESIAN_POINT ( 'NONE',  ( -20.85369094651513677, -107.5158378249862352, -5.057062608101891676 ) ) ;
#2616=MANIFOLD_SOLID_BREP ( 'Stock-MAS-672-1', #6319 ) ;
#2620=CYLINDRICAL_SURFACE ( 'NONE', #481, 6.000000000000000000 ) ;
#2695=CARTESIAN_POINT ( 'NONE',  ( -20.87112600995945755, -109.7258744763782943, -5.497689735156006563 ) ) ;
#2699=ORIENTED_EDGE ( 'NONE', *, *, #4522, .T. ) ;
#2705=CARTESIAN_POINT ( 'NONE',  ( -12.99052370552812796, -91.62169785875414618, -10.25852757147468708 ) ) ;
#2706=AXIS2_PLACEMENT_3D ( 'NONE', #4840, #7031, #9344 ) ;
#2739=DIRECTION ( 'NONE',  ( 1.000000000000000078E-15, -1.000000000000000000, 0.000000000000000000 ) ) ;
#2801=CARTESIAN_POINT ( 'NONE',  ( -20.86293661740132421, -106.0955903196376227, -5.852253362411212301 ) ) ;
#2828=ORIENTED_EDGE ( 'NONE', *, *, #13827, .F. ) ;
#2852=SHAPE_REPRESENTATION ( 'Boring Bar Holder', ( #6789 ), #5587 ) ;
#2861=EDGE_CURVE ( 'NONE', #11125, #12515, #10163, .T. ) ;
#2942=VERTEX_POINT ( 'NONE', #160 ) ;
#2949=CARTESIAN_POINT ( 'NONE',  ( -20.79204332525751653, -106.1260846184876385, -6.431863631274442383 ) ) ;
#2951=DIRECTION ( 'NONE',  ( -1.000000000000000000, 0.000000000000000000, -1.011922027653137143E-15 ) ) ;
#3010=DIRECTION ( 'NONE',  ( 1.000000000000000078E-15, 0.000000000000000000, -1.000000000000000000 ) ) ;
#3020=AXIS2_PLACEMENT_3D ( 'NONE', #1127, #10309, #13834 ) ;
#3034=CIRCLE ( 'NONE', #3020, 1.075000000000000400 ) ;
#3044=FACE_OUTER_BOUND ( 'NONE', #4911, .T. ) ;
#3045=PLANE ( 'NONE',  #9471 ) ;
#3054=CARTESIAN_POINT ( 'NONE',  ( -100.5053766806731090, -107.1622034095863825, -7.162689735156084758 ) ) ;
#3090=VERTEX_POINT ( 'NONE', #3196 ) ;
#3094=CARTESIAN_POINT ( 'NONE',  ( -9.499699860810999041, -27.00737899243799234, -5.497689735155994128 ) ) ;
#3196=CARTESIAN_POINT ( 'NONE',  ( -20.84918524500973191, -107.1622034095862972, -5.012689735156006243 ) ) ;
#3199=CARTESIAN_POINT ( 'NONE',  ( -13.40858384722878505, -91.95517843101794142, -0.5497938619115086967 ) ) ;
#3238=CARTESIAN_POINT ( 'NONE',  ( -20.60655739512266749, -107.1622034095862972, -7.162689735156005710 ) ) ;
#3240=VECTOR ( 'NONE', #9476, 1000.000000000000000 ) ;
#3250=DIRECTION ( 'NONE',  ( 1.000000000000000078E-15, 0.000000000000000000, -1.000000000000000000 ) ) ;
#3255=CARTESIAN_POINT ( 'NONE',  ( -10.46773630126042498, -90.58249387939251562, -7.400451369742719443 ) ) ;
#3262=CARTESIAN_POINT ( 'NONE',  ( -20.87112600995945755, -110.0073789924380065, -5.497689735156006563 ) ) ;
#3279=CARTESIAN_POINT ( 'NONE',  ( -14.55020162889266899, -93.22838571284465559, -0.2054526157817354315 ) ) ;
#3285=ORIENTED_EDGE ( 'NONE', *, *, #2861, .F. ) ;
#3298=ORIENTED_EDGE ( 'NONE', *, *, #12649, .T. ) ;
#3309=CARTESIAN_POINT ( 'NONE',  ( -20.86505398763562269, -106.5010658813280742, -5.235401919846907504 ) ) ;
#3320=CARTESIAN_POINT ( 'NONE',  ( -18.09969986081092230, -101.1019538585846931, -6.399987709240088307 ) ) ;
#3324=CARTESIAN_POINT ( 'NONE',  ( -10.62602584962065855, -90.61080531379087688, -7.756162395898620332 ) ) ;
#3326=EDGE_CURVE ( 'NONE', #11125, #2288, #12921, .T. ) ;
#3348=CARTESIAN_POINT ( 'NONE',  ( -14.84558095633615515, -93.78297125096656828, -0.1661650273432554725 ) ) ;
#3375=VERTEX_POINT ( 'NONE', #9303 ) ;
#3383=VECTOR ( 'NONE', #2368, 1000.000000000000000 ) ;
#3384=CARTESIAN_POINT ( 'NONE',  ( -20.84918524500973902, -106.9855902083963173, -5.012689735156002691 ) ) ;
#3393=EDGE_LOOP ( 'NONE', ( #5436, #8272, #6501 ) ) ;
#3440=CARTESIAN_POINT ( 'NONE',  ( -20.82328182105635150, -108.2441250888176256, -6.239265671067229846 ) ) ;
#3444=PRODUCT_DEFINITION_CONTEXT ( 'detailed design', #13204, 'design' ) ;
#3469=EDGE_CURVE ( 'NONE', #3791, #2288, #7307, .T. ) ;
#3472=LINE ( 'NONE', #1178, #3784 ) ;
#3501=CARTESIAN_POINT ( 'NONE',  ( -11.11913394994981807, -90.72833461817117495, -2.380443756164408509 ) ) ;
#3509=DIRECTION ( 'NONE',  ( 1.000000000000000078E-15, -1.000000000000000000, 0.000000000000000000 ) ) ;
#3521=VERTEX_POINT ( 'NONE', #7564 ) ;
#3552=CARTESIAN_POINT ( 'NONE',  ( -11.88635259617872819, -91.00826541128077452, -9.472131609326678969 ) ) ;
#3561=ORIENTED_EDGE ( 'NONE', *, *, #3469, .F. ) ;
#3568=VECTOR ( 'NONE', #1054, 1000.000000000000000 ) ;
#3610=( LENGTH_UNIT ( ) NAMED_UNIT ( * ) SI_UNIT ( .MILLI., .METRE. ) );
#3625=AXIS2_PLACEMENT_3D ( 'NONE', #2292, #3509, #5795 ) ;
#3638=VERTEX_POINT ( 'NONE', #14391 ) ;
#3704=CARTESIAN_POINT ( 'NONE',  ( -10.96448334217298282, -90.68610839286715475, -8.382549063897425157 ) ) ;
#3737=ORIENTED_EDGE ( 'NONE', *, *, #303, .F. ) ;
#3752=ORIENTED_EDGE ( 'NONE', *, *, #14899, .F. ) ;
#3784=VECTOR ( 'NONE', #14798, 1000.000000000000000 ) ;
#3790=ORIENTED_EDGE ( 'NONE', *, *, #4522, .F. ) ;
#3791=VERTEX_POINT ( 'NONE', #8937 ) ;
#3845=CARTESIAN_POINT ( 'NONE',  ( -15.49969986081092621, -96.50737899243799234, -9.210188241073819171 ) ) ;
#3854=CARTESIAN_POINT ( 'NONE',  ( -11.91715604007085716, -91.02193864445173688, -9.500011814598602555 ) ) ;
#3855=CARTESIAN_POINT ( 'NONE',  ( -15.49969986081094042, -85.00737899243800655, -5.497689735156000346 ) ) ;
#3858=EDGE_LOOP ( 'NONE', ( #4639, #5418, #1514, #4219 ) ) ;
#3961=ORIENTED_EDGE ( 'NONE', *, *, #5810, .F. ) ;
#3970=CIRCLE ( 'NONE', #4950, 6.000000000000000000 ) ;
#3981=ORIENTED_EDGE ( 'NONE', *, *, #10600, .F. ) ;
#4047=EDGE_LOOP ( 'NONE', ( #13813, #10275, #14082, #4241 ) ) ;
#4201=FACE_OUTER_BOUND ( 'NONE', #12347, .T. ) ;
#4219=ORIENTED_EDGE ( 'NONE', *, *, #9952, .F. ) ;
#4241=ORIENTED_EDGE ( 'NONE', *, *, #10600, .T. ) ;
#4263=FACE_OUTER_BOUND ( 'NONE', #13074, .T. ) ;
#4273=FACE_OUTER_BOUND ( 'NONE', #8486, .T. ) ;
#4312=ORIENTED_EDGE ( 'NONE', *, *, #2030, .F. ) ;
#4316=PLANE ( 'NONE',  #6385 ) ;
#4334=CIRCLE ( 'NONE', #10183, 1.075000000000000400 ) ;
#4341=CARTESIAN_POINT ( 'NONE',  ( -14.84437367148764686, -93.78075803281299727, -10.82899037021154953 ) ) ;
#4381=CARTESIAN_POINT ( 'NONE',  ( 0.000000000000000000, 0.000000000000000000, 0.000000000000000000 ) ) ;
#4401=CARTESIAN_POINT ( 'NONE',  ( -10.13128693740209840, -90.53913777082694025, -5.691719241778902649 ) ) ;
#4432=AXIS2_PLACEMENT_3D ( 'NONE', #13675, #8922, #13601 ) ;
#4437=DIRECTION ( 'NONE',  ( 1.000000000000000078E-15, -1.000000000000000000, 0.000000000000000000 ) ) ;
#4455=VECTOR ( 'NONE', #7008, 1000.000000000000114 ) ;
#4515=LINE ( 'NONE', #13843, #4455 ) ;
#4522=EDGE_CURVE ( 'NONE', #11878, #9733, #1649, .T. ) ;
#4525=CARTESIAN_POINT ( 'NONE',  ( -9.499699860810959962, -67.00737899243799234, -5.497689735155994128 ) ) ;
#4574=CARTESIAN_POINT ( 'NONE',  ( -10.31310630199996403, -90.56276996998271045, -4.100613025930020861 ) ) ;
#4609=CARTESIAN_POINT ( 'NONE',  ( -20.87112600995945755, -108.0608273576312968, -5.497689735156002122 ) ) ;
#4639=ORIENTED_EDGE ( 'NONE', *, *, #8932, .F. ) ;
#4642=ORIENTED_EDGE ( 'NONE', *, *, #1720, .F. ) ;
#4653=CARTESIAN_POINT ( 'NONE',  ( -10.32812483352770450, -90.56483419681595137, -4.046006962230706883 ) ) ;
#4669=CARTESIAN_POINT ( 'NONE',  ( -20.86311301939802831, -108.2285642389760483, -5.850193701754826670 ) ) ;
#4748=ADVANCED_FACE ( 'NONE', ( #7349 ), #2620, .T. ) ;
#4758=AXIS2_PLACEMENT_3D ( 'NONE', #3855, #2481, #7363 ) ;
#4795=ORIENTED_EDGE ( 'NONE', *, *, #7194, .F. ) ;
#4799=PRODUCT_DEFINITION ( 'UNKNOWN', '', #11954, #3444 ) ;
#4840=CARTESIAN_POINT ( 'NONE',  ( -9.499699860810929763, -96.50737899243799234, -5.497689735155988799 ) ) ;
#4844=FACE_OUTER_BOUND ( 'NONE', #8759, .T. ) ;
#4859=CARTESIAN_POINT ( 'NONE',  ( -10.81589814721888665, -90.65038570870460433, -8.129004277159287639 ) ) ;
#4911=EDGE_LOOP ( 'NONE', ( #11862, #14117, #7063, #3790, #9740 ) ) ;
#4950=AXIS2_PLACEMENT_3D ( 'NONE', #12225, #2739, #9778 ) ;
#4964=SURFACE_STYLE_FILL_AREA ( #11917 ) ;
#5004=CARTESIAN_POINT ( 'NONE',  ( -15.27714973199592485, -94.62907795360041519, -10.37839032168656672 ) ) ;
#5014=AXIS2_PLACEMENT_3D ( 'NONE', #1989, #4437, #690 ) ;
#5112=ORIENTED_EDGE ( 'NONE', *, *, #10743, .T. ) ;
#5139=VERTEX_POINT ( 'NONE', #10847 ) ;
#5165=CARTESIAN_POINT ( 'NONE',  ( -20.61091276329630162, -106.9682996518086497, -7.149495196850712553 ) ) ;
#5199=ORIENTED_EDGE ( 'NONE', *, *, #3469, .T. ) ;
#5215=VECTOR ( 'NONE', #11216, 1000.000000000000000 ) ;
#5246=CARTESIAN_POINT ( 'NONE',  ( -20.72174206363053273, -106.3077111449690619, -6.767278426752862508 ) ) ;
#5261=CARTESIAN_POINT ( 'NONE',  ( -21.49969986081095996, -67.00737899243799234, -5.497689735156006563 ) ) ;
#5285=EDGE_LOOP ( 'NONE', ( #2472, #13798, #7989, #10603 ) ) ;
#5289=CARTESIAN_POINT ( 'NONE',  ( -18.09969986081091164, -109.9722034095862995, -10.19792577984107318 ) ) ;
#5316=ADVANCED_FACE ( 'NONE', ( #10447 ), #12520, .F. ) ;
#5339=CIRCLE ( 'NONE', #1668, 6.000000000000001776 ) ;
#5418=ORIENTED_EDGE ( 'NONE', *, *, #11972, .T. ) ;
#5436=ORIENTED_EDGE ( 'NONE', *, *, #303, .T. ) ;
#5561=CARTESIAN_POINT ( 'NONE',  ( -11.66301194181331979, -90.91152723309099315, -1.736239442649727627 ) ) ;
#5587=( GEOMETRIC_REPRESENTATION_CONTEXT ( 3 ) GLOBAL_UNCERTAINTY_ASSIGNED_CONTEXT ( ( #7099 ) ) GLOBAL_UNIT_ASSIGNED_CONTEXT ( ( #3610, #6115, #12877 ) ) REPRESENTATION_CONTEXT ( 'NONE', 'WORKASPACE' ) );
#5590=EDGE_LOOP ( 'NONE', ( #3961, #3752, #12160, #4795 ) ) ;
#5612=CARTESIAN_POINT ( 'NONE',  ( -10.35395692991667360, -90.56631534932571981, -7.082904691259424901 ) ) ;
#5618=ADVANCED_FACE ( 'NONE', ( #12501, #7743 ), #4316, .T. ) ;
#5637=CARTESIAN_POINT ( 'NONE',  ( -10.12676381431746542, -90.53940471697117687, -5.497640657892870486 ) ) ;
#5655=ORIENTED_EDGE ( 'NONE', *, *, #13938, .T. ) ;
#5714=CARTESIAN_POINT ( 'NONE',  ( -11.75214016307909581, -90.94766999248710704, -1.647608471205698644 ) ) ;
#5746=CYLINDRICAL_SURFACE ( 'NONE', #12591, 6.000000000000000000 ) ;
#5757=B_SPLINE_CURVE_WITH_KNOTS ( 'NONE', 3,
 ( #15067, #12790, #1140, #12944, #10631, #2524, #3440, #4669, #7175, #9248 ),
 .UNSPECIFIED., .F., .F.,
 ( 4, 2, 2, 2, 4 ),
 ( 0.000000000000000000, 0.0005837886004704026912, 0.001167577200940805382, 0.001751365801411208182, 0.002335154401881610765 ),
 .UNSPECIFIED. ) ;
#5758=DIRECTION ( 'NONE',  ( 1.000000000000000000, 1.000000000000000078E-15, 1.000000000000000078E-15 ) ) ;
#5761=CARTESIAN_POINT ( 'NONE',  ( -10.12827359990930987, -90.53873857836721584, -5.509565971075029545 ) ) ;
#5784=CARTESIAN_POINT ( 'NONE',  ( -10.14594238360923129, -90.54069878331144139, -4.997746991299526265 ) ) ;
#5795=DIRECTION ( 'NONE',  ( -1.000000000000000000, 0.000000000000000000, -9.688619527525975741E-16 ) ) ;
#5810=EDGE_CURVE ( 'NONE', #2175, #12515, #6330, .T. ) ;
#5857=CARTESIAN_POINT ( 'NONE',  ( -10.32306602483566316, -90.56413277834681708, -4.064149291360593885 ) ) ;
#5887=CARTESIAN_POINT ( 'NONE',  ( -20.84918524500973191, -107.1622034095862972, -5.012689735156006243 ) ) ;
#5908=CARTESIAN_POINT ( 'NONE',  ( -11.97891935325373147, -91.04984766112443140, -9.554806339755154809 ) ) ;
#5992=ORIENTED_EDGE ( 'NONE', *, *, #13827, .T. ) ;
#6026=EDGE_LOOP ( 'NONE', ( #1636, #12125, #9968, #5199 ) ) ;
#6081=CARTESIAN_POINT ( 'NONE',  ( -15.49969986081092088, -110.0073789924380065, -0.1262635860074601546 ) ) ;
#6098=ORIENTED_EDGE ( 'NONE', *, *, #12649, .F. ) ;
#6115=( NAMED_UNIT ( * ) PLANE_ANGLE_UNIT ( ) SI_UNIT ( $, .RADIAN. ) );
#6278=CARTESIAN_POINT ( 'NONE',  ( -15.49969986081095996, -67.00737899243799234, -5.497689735156000346 ) ) ;
#6296=CARTESIAN_POINT ( 'NONE',  ( -15.49969986081092266, -109.4443699603185109, -0.1262635860074601546 ) ) ;
#6305=CARTESIAN_POINT ( 'NONE',  ( -20.68283285135230898, -106.4450808729558560, -6.911160851980194586 ) ) ;
#6319=CLOSED_SHELL ( 'NONE', ( #12229, #6986, #880, #10763, #1591, #5316, #5618, #2343, #7205, #4748, #8844, #7972, #9455, #12992 ) ) ;
#6330=( BOUNDED_CURVE ( )  B_SPLINE_CURVE ( 3, ( #1555, #5004, #10965, #3845 ),
 .UNSPECIFIED., .F., .T. ) 
 B_SPLINE_CURVE_WITH_KNOTS ( ( 4, 4 ),
 ( 0.7562501201432320075, 1.227990006496096020 ),
 .UNSPECIFIED. ) 
 CURVE ( )  GEOMETRIC_REPRESENTATION_ITEM ( )  RATIONAL_B_SPLINE_CURVE ( ( 1.000000000000000000, 0.9815409421278752378, 0.9815409421278752378, 1.000000000000000000 ) ) 
 REPRESENTATION_ITEM ( '' )  );
#6351=DIRECTION ( 'NONE',  ( -1.000000000000000078E-15, 1.000000000000000000, 0.000000000000000000 ) ) ;
#6385=AXIS2_PLACEMENT_3D ( 'NONE', #3320, #5758, #3250 ) ;
#6444=CARTESIAN_POINT ( 'NONE',  ( -18.09969986081091875, -107.1622034095862972, -5.012689735156002691 ) ) ;
#6486=CARTESIAN_POINT ( 'NONE',  ( -28.40830458780451551, -109.6305988279009966, -3.679722063549803135 ) ) ;
#6487=CARTESIAN_POINT ( 'NONE',  ( -18.09969986081092586, -95.91433005893298969, -10.19792577984107318 ) ) ;
#6501=ORIENTED_EDGE ( 'NONE', *, *, #7464, .T. ) ;
#6523=CARTESIAN_POINT ( 'NONE',  ( -20.62737807198738693, -106.7814035276991120, -7.097650603566109773 ) ) ;
#6529=LINE ( 'NONE', #12510, #5215 ) ;
#6541=LINE ( 'NONE', #746, #13712 ) ;
#6542=B_SPLINE_CURVE_WITH_KNOTS ( 'NONE', 3,
 ( #4609, #8187, #98, #2612, #9263, #5887 ),
 .UNSPECIFIED., .F., .F.,
 ( 4, 2, 4 ),
 ( 0.002335154401881610765, 0.002868089949059464579, 0.003401025496237318393 ),
 .UNSPECIFIED. ) ;
#6581=CARTESIAN_POINT ( 'NONE',  ( -15.49969986081092088, -109.4789632527123047, -0.7863429266504098347 ) ) ;
#6582=VERTEX_POINT ( 'NONE', #1238 ) ;
#6686=CARTESIAN_POINT ( 'NONE',  ( -20.87112600995945755, -109.7258744763782943, -5.497689735156006563 ) ) ;
#6691=ORIENTED_EDGE ( 'NONE', *, *, #5810, .T. ) ;
#6702=CARTESIAN_POINT ( 'NONE',  ( -11.53159268371330093, -90.86154151202431706, -1.876852786247884985 ) ) ;
#6721=LINE ( 'NONE', #12714, #14739 ) ;
#6728=CARTESIAN_POINT ( 'NONE',  ( -20.87112600995946110, -106.2635794615412834, -5.497689735156005675 ) ) ;
#6763=DIRECTION ( 'NONE',  ( 1.000000000000000000, 1.000000000000000078E-15, 1.000000000000000078E-15 ) ) ;
#6774=CARTESIAN_POINT ( 'NONE',  ( -13.79377835810313613, -92.30760736031301406, -0.4016677776517476595 ) ) ;
#6778=VERTEX_POINT ( 'NONE', #6487 ) ;
#6789=AXIS2_PLACEMENT_3D ( 'NONE', #4381, #12419, #6809 ) ;
#6806=CARTESIAN_POINT ( 'NONE',  ( -19.85327209184728758, -109.9213672076435131, -9.227913261884630458 ) ) ;
#6809=DIRECTION ( 'NONE',  ( 1.000000000000000000, 0.000000000000000000, 0.000000000000000000 ) ) ;
#6852=CARTESIAN_POINT ( 'NONE',  ( -13.36723182930882103, -91.92030416804652759, -0.5674792550076069864 ) ) ;
#6969=CARTESIAN_POINT ( 'NONE',  ( -10.12903334873179517, -90.53886212111028442, -5.595198070896032938 ) ) ;
#6986=ADVANCED_FACE ( 'NONE', ( #9569 ), #5746, .T. ) ;
#6987=MECHANICAL_DESIGN_GEOMETRIC_PRESENTATION_REPRESENTATION('',(#13611),#14357);
#6988=EDGE_CURVE ( 'NONE', #3638, #3090, #6542, .T. ) ;
#7006=AXIS2_PLACEMENT_3D ( 'NONE', #1125, #8074, #2127 ) ;
#7008=DIRECTION ( 'NONE',  ( -2.940315329303969755E-16, 0.8386705679454240503, -0.5446390350150269732 ) ) ;
#7031=DIRECTION ( 'NONE',  ( 1.000000000000000078E-15, 0.000000000000000000, -1.000000000000000000 ) ) ;
#7035=( BOUNDED_CURVE ( )  B_SPLINE_CURVE ( 3, ( #8066, #14742, #11445, #4341 ),
 .UNSPECIFIED., .F., .F. ) 
 B_SPLINE_CURVE_WITH_KNOTS ( ( 4, 4 ),
 ( 5.550165736622670209, 6.177741627597179708 ),
 .UNSPECIFIED. ) 
 CURVE ( )  GEOMETRIC_REPRESENTATION_ITEM ( )  RATIONAL_B_SPLINE_CURVE ( ( 1.000000000000000000, 0.9674474632520878581, 0.9674474632520878581, 1.000000000000000000 ) ) 
 REPRESENTATION_ITEM ( '' )  );
#7052=CARTESIAN_POINT ( 'NONE',  ( -11.39494938265116453, -90.81200083036684134, -8.981479305044373973 ) ) ;
#7059=LINE ( 'NONE', #3262, #14504 ) ;
#7063=ORIENTED_EDGE ( 'NONE', *, *, #10301, .F. ) ;
#7099=UNCERTAINTY_MEASURE_WITH_UNIT (LENGTH_MEASURE( 1.000000000000000082E-05 ), #3610, 'distance_accuracy_value', 'NONE');
#7129=CARTESIAN_POINT ( 'NONE',  ( -13.26641246986315359, -91.82643169460182264, -10.39079603009238006 ) ) ;
#7175=CARTESIAN_POINT ( 'NONE',  ( -20.87112600995946110, -108.1670994135940020, -5.659551793623918137 ) ) ;
#7178=ORIENTED_EDGE ( 'NONE', *, *, #14109, .F. ) ;
#7189=VECTOR ( 'NONE', #13472, 1000.000000000000000 ) ;
#7194=EDGE_CURVE ( 'NONE', #12515, #3791, #9797, .T. ) ;
#7205=ADVANCED_FACE ( 'NONE', ( #10798 ), #328, .F. ) ;
#7208=CARTESIAN_POINT ( 'NONE',  ( -14.84437367148764686, -93.78075803281299727, -10.82899037021154953 ) ) ;
#7212=ORIENTED_EDGE ( 'NONE', *, *, #302, .T. ) ;
#7307=LINE ( 'NONE', #6081, #8930 ) ;
#7349=FACE_OUTER_BOUND ( 'NONE', #4047, .T. ) ;
#7363=DIRECTION ( 'NONE',  ( -1.000000000000000000, 0.000000000000000000, -9.688619527525975741E-16 ) ) ;
#7369=CARTESIAN_POINT ( 'NONE',  ( -14.84437367148764686, -93.78075803281299727, -10.82899037021154953 ) ) ;
#7393=( LENGTH_UNIT ( ) NAMED_UNIT ( * ) SI_UNIT ( .MILLI., .METRE. ) );
#7464=EDGE_CURVE ( 'NONE', #3375, #11878, #3472, .T. ) ;
#7564=CARTESIAN_POINT ( 'NONE',  ( -21.49969986081095996, -67.00737899243799234, -5.497689735156006563 ) ) ;
#7607=VECTOR ( 'NONE', #7718, 1000.000000000000000 ) ;
#7667=ORIENTED_EDGE ( 'NONE', *, *, #14899, .T. ) ;
#7699=PLANE ( 'NONE',  #7006 ) ;
#7718=DIRECTION ( 'NONE',  ( -1.000000000000000078E-15, 1.000000000000000000, 0.000000000000000000 ) ) ;
#7743=FACE_BOUND ( 'NONE', #1902, .T. ) ;
#7818=CARTESIAN_POINT ( 'NONE',  ( -10.19146053163822963, -90.54589302285323527, -6.344455741628062029 ) ) ;
#7827=EDGE_CURVE ( 'NONE', #3090, #2942, #752, .T. ) ;
#7878=CARTESIAN_POINT ( 'NONE',  ( -20.87112600995945400, -109.8308986703933812, -7.501670736676251394 ) ) ;
#7927=CARTESIAN_POINT ( 'NONE',  ( -10.30965874483576883, -90.56230343551661122, -4.113522448036712298 ) ) ;
#7929=DIRECTION ( 'NONE',  ( 0.1908089953765451374, -0.5346324819374546067, -0.8232618274527192526 ) ) ;
#7972=ADVANCED_FACE ( 'NONE', ( #2392 ), #250, .F. ) ;
#7985=CARTESIAN_POINT ( 'NONE',  ( -15.49969986081092266, -109.4443699603185109, -0.1262635860074601546 ) ) ;
#7989=ORIENTED_EDGE ( 'NONE', *, *, #14873, .T. ) ;
#8001=CARTESIAN_POINT ( 'NONE',  ( -12.20226299988479646, -91.14247851622610597, -1.229095371057126629 ) ) ;
#8066=CARTESIAN_POINT ( 'NONE',  ( -18.09969986081092586, -95.91433005893298969, -10.19792577984107318 ) ) ;
#8074=DIRECTION ( 'NONE',  ( -9.462935785116304784E-16, 0.9986295347545739443, -0.05233595624294359872 ) ) ;
#8114=( BOUNDED_CURVE ( )  B_SPLINE_CURVE ( 3, ( #6686, #10522, #971, #7985 ),
 .UNSPECIFIED., .F., .F. ) 
 B_SPLINE_CURVE_WITH_KNOTS ( ( 4, 4 ),
 ( 4.712388980384689674, 6.283185307179586232 ),
 .UNSPECIFIED. ) 
 CURVE ( )  GEOMETRIC_REPRESENTATION_ITEM ( )  RATIONAL_B_SPLINE_CURVE ( ( 1.000000000000000000, 0.8047378541243649375, 0.8047378541243649375, 1.000000000000000000 ) ) 
 REPRESENTATION_ITEM ( '' )  );
#8152=EDGE_CURVE ( 'NONE', #11125, #3375, #10878, .T. ) ;
#8158=CARTESIAN_POINT ( 'NONE',  ( -12.57554303975000742, -91.34342846084412315, -0.9737555918262782439 ) ) ;
#8167=LINE ( 'NONE', #12856, #3383 ) ;
#8181=DIRECTION ( 'NONE',  ( -1.000000000000000078E-15, 1.000000000000000000, 0.000000000000000000 ) ) ;
#8187=CARTESIAN_POINT ( 'NONE',  ( -20.87112600995946110, -107.9638125199853533, -5.349927266640145618 ) ) ;
#8215=CARTESIAN_POINT ( 'NONE',  ( -10.12676381431746542, -90.53940471697117687, -5.497640657892870486 ) ) ;
#8225=CONICAL_SURFACE ( 'NONE', #1399, 6.000000000000001776, 0.03490658503988566114 ) ;
#8272=ORIENTED_EDGE ( 'NONE', *, *, #13938, .F. ) ;
#8415=ORIENTED_EDGE ( 'NONE', *, *, #13571, .T. ) ;
#8486=EDGE_LOOP ( 'NONE', ( #3298, #6691, #3285, #10409, #5655 ) ) ;
#8521=FACE_OUTER_BOUND ( 'NONE', #6026, .T. ) ;
#8541=DIRECTION ( 'NONE',  ( -1.000000000000000000, 0.000000000000000000, -1.011922027653137143E-15 ) ) ;
#8603=ORIENTED_EDGE ( 'NONE', *, *, #6988, .T. ) ;
#8609=CARTESIAN_POINT ( 'NONE',  ( -20.87112600995946110, -106.2635794615412834, -5.497689735156005675 ) ) ;
#8622=SURFACE_STYLE_USAGE ( .BOTH. , #447 ) ;
#8628=CARTESIAN_POINT ( 'NONE',  ( -20.87112600995945755, -110.0073789924380065, -5.497689735156006563 ) ) ;
#8693=CARTESIAN_POINT ( 'NONE',  ( -15.49969986081092621, -96.50737899243799234, -9.210188241073819171 ) ) ;
#8698=LINE ( 'NONE', #5261, #12457 ) ;
#8755=UNCERTAINTY_MEASURE_WITH_UNIT (LENGTH_MEASURE( 1.000000000000000082E-05 ), #7393, 'distance_accuracy_value', 'NONE');
#8759=EDGE_LOOP ( 'NONE', ( #7178, #1006, #3561, #15089, #8415, #7212, #4312, #14824, #933 ) ) ;
#8778=VERTEX_POINT ( 'NONE', #12155 ) ;
#8844=ADVANCED_FACE ( 'NONE', ( #3044 ), #7699, .F. ) ;
#8847=EDGE_CURVE ( 'NONE', #3791, #2017, #8924, .T. ) ;
#8858=CARTESIAN_POINT ( 'NONE',  ( -15.49969986081091555, -110.0073789924380065, -5.497689735156000346 ) ) ;
#8922=DIRECTION ( 'NONE',  ( 1.000000000000000000, 1.000000000000000078E-15, 1.000000000000000078E-15 ) ) ;
#8924=B_SPLINE_CURVE_WITH_KNOTS ( 'NONE', 3,
 ( #10385, #9154, #11609, #11458, #2054, #14825, #9079, #13684, #9306, #3348, #2204, #3279, #13830, #6774, #9230, #3199, #6852, #12690, #13980, #15048, #8158, #8001, #5714, #5561, #6702, #9004, #11382, #13757, #11533, #3501, #10234, #12537, #4653, #5857, #4574, #7927, #984, #12848, #12771, #12615, #5784, #2359, #5637 ),
 .UNSPECIFIED., .F., .F.,
 ( 4, 2, 2, 2, 2, 2, 2, 2, 2, 1, 2, 2, 2, 2, 2, 2, 2, 2, 2, 1, 1, 2, 4 ),
 ( 0.000000000000000000, 0.07105225421133361252, 0.1065783813170013972, 0.1243414448698352825, 0.1332229766462521836, 0.1421045084226690847, 0.2131567626339919419, 0.2486828897396533844, 0.2575644215160691197, 0.2664459532924848828, 0.2842090168453164090, 0.3552612710566459553, 0.3730243346094782586, 0.3819058663858942992, 0.3907873981623103399, 0.4263135252679747245, 0.4973657794793031051, 0.4995861624234071430, 0.5018065453675111254, 0.5062473112557193122, 0.5151288430321355749, 0.5328919065849679892, 0.5684180336906330400 ),
 .UNSPECIFIED. ) ;
#8930=VECTOR ( 'NONE', #10765, 1000.000000000000000 ) ;
#8932=EDGE_CURVE ( 'NONE', #3521, #8778, #434, .T. ) ;
#8937=CARTESIAN_POINT ( 'NONE',  ( -15.49969986081093509, -96.50737899243799234, -0.1262635860074601546 ) ) ;
#8943=CARTESIAN_POINT ( 'NONE',  ( -21.49969986081099904, -27.00737899243800655, -5.497689735156007451 ) ) ;
#8994=CYLINDRICAL_SURFACE ( 'NONE', #4432, 1.074999999999999512 ) ;
#9004=CARTESIAN_POINT ( 'NONE',  ( -11.50449320635804007, -90.85166671083230483, -1.907031398356576979 ) ) ;
#9019=DIRECTION ( 'NONE',  ( -2.940315329303969755E-16, 0.8386705679454240503, -0.5446390350150269732 ) ) ;
#9051=CARTESIAN_POINT ( 'NONE',  ( -10.15458489671155640, -90.54171561441047800, -6.038535867389205336 ) ) ;
#9079=CARTESIAN_POINT ( 'NONE',  ( -15.00778987199241143, -94.12399836386714469, -0.1485842411706335409 ) ) ;
#9107=EDGE_CURVE ( 'NONE', #2245, #5139, #4334, .T. ) ;
#9112=CARTESIAN_POINT ( 'NONE',  ( -20.86213698926522397, -106.5729322520875968, -5.184177647451607029 ) ) ;
#9128=CARTESIAN_POINT ( 'NONE',  ( -10.14011164466803017, -90.54012419075833407, -5.881547205074356910 ) ) ;
#9154=CARTESIAN_POINT ( 'NONE',  ( -15.49962021429866255, -96.00462026634728829, -0.1262635860074601823 ) ) ;
#9209=DIRECTION ( 'NONE',  ( -1.000000000000000078E-15, 1.000000000000000000, 0.000000000000000000 ) ) ;
#9229=ORIENTED_EDGE ( 'NONE', *, *, #749, .T. ) ;
#9230=CARTESIAN_POINT ( 'NONE',  ( -13.62642369053113356, -92.14448157524431338, -0.4599730570185335266 ) ) ;
#9248=CARTESIAN_POINT ( 'NONE',  ( -20.87112600995945755, -108.0608273576312968, -5.497689735156002122 ) ) ;
#9263=CARTESIAN_POINT ( 'NONE',  ( -20.84918524500973191, -107.3388303236057624, -5.012689735156009796 ) ) ;
#9285=DIRECTION ( 'NONE',  ( -1.000000000000000000, -1.156482317317871331E-15, -1.011922027653137537E-15 ) ) ;
#9303=CARTESIAN_POINT ( 'NONE',  ( -18.09969986081091875, -109.5095050892490889, -1.369115884304552999 ) ) ;
#9306=CARTESIAN_POINT ( 'NONE',  ( -14.90205750506880378, -93.89666313514172202, -0.1595392253041037489 ) ) ;
#9341=VECTOR ( 'NONE', #10158, 1000.000000000000000 ) ;
#9344=DIRECTION ( 'NONE',  ( -1.000000000000000000, 0.000000000000000000, -1.011922027653137537E-15 ) ) ;
#9437=CARTESIAN_POINT ( 'NONE',  ( -12.10298406914416525, -91.10791589579226013, -9.660565934256062803 ) ) ;
#9455=ADVANCED_FACE ( 'NONE', ( #8521 ), #12275, .T. ) ;
#9471=AXIS2_PLACEMENT_3D ( 'NONE', #607, #7929, #10003 ) ;
#9476=DIRECTION ( 'NONE',  ( -1.000000000000000078E-15, 1.000000000000000000, 0.000000000000000000 ) ) ;
#9506=ORIENTED_EDGE ( 'NONE', *, *, #1401, .F. ) ;
#9569=FACE_OUTER_BOUND ( 'NONE', #3858, .T. ) ;
#9665=PRODUCT_DEFINITION_SHAPE ( 'NONE', 'NONE',  #4799 ) ;
#9693=EDGE_LOOP ( 'NONE', ( #11262, #1422, #9950, #5992, #12057 ) ) ;
#9708=CARTESIAN_POINT ( 'NONE',  ( -15.49969986081091555, -110.0073789924380065, -5.497689735156000346 ) ) ;
#9733=VERTEX_POINT ( 'NONE', #2695 ) ;
#9740=ORIENTED_EDGE ( 'NONE', *, *, #7464, .F. ) ;
#9778=DIRECTION ( 'NONE',  ( -1.000000000000000000, -1.156482317317871331E-15, -1.011922027653137537E-15 ) ) ;
#9797=LINE ( 'NONE', #14462, #7189 ) ;
#9838=CARTESIAN_POINT ( 'NONE',  ( -20.60655739512266749, -107.0640443292477073, -7.162689735156005710 ) ) ;
#9950=ORIENTED_EDGE ( 'NONE', *, *, #14766, .T. ) ;
#9952=EDGE_CURVE ( 'NONE', #8778, #14720, #12560, .T. ) ;
#9961=APPLICATION_CONTEXT ( 'automotive_design' ) ;
#9968=ORIENTED_EDGE ( 'NONE', *, *, #7194, .T. ) ;
#10003=DIRECTION ( 'NONE',  ( -0.9418150828622243731, -0.3361314470459753623, -9.418150828622246992E-16 ) ) ;
#10050=DIRECTION ( 'NONE',  ( -1.000000000000000078E-15, 1.000000000000000000, 0.000000000000000000 ) ) ;
#10158=DIRECTION ( 'NONE',  ( 1.000000000000000000, 1.000000000000000078E-15, 1.000000000000000078E-15 ) ) ;
#10160=VECTOR ( 'NONE', #9019, 1000.000000000000114 ) ;
#10163=LINE ( 'NONE', #14840, #10160 ) ;
#10183=AXIS2_PLACEMENT_3D ( 'NONE', #11143, #1728, #10914 ) ;
#10233=ORIENTED_EDGE ( 'NONE', *, *, #9107, .T. ) ;
#10234=CARTESIAN_POINT ( 'NONE',  ( -10.73868464545405921, -90.63222195594610753, -2.967393652951166860 ) ) ;
#10275=ORIENTED_EDGE ( 'NONE', *, *, #14873, .F. ) ;
#10301=EDGE_CURVE ( 'NONE', #9733, #2288, #8114, .T. ) ;
#10309=DIRECTION ( 'NONE',  ( -1.000000000000000000, -1.000000000000000078E-15, -1.000000000000000078E-15 ) ) ;
#10385=CARTESIAN_POINT ( 'NONE',  ( -15.49969986081093509, -96.50737899243799234, -0.1262635860074601546 ) ) ;
#10409=ORIENTED_EDGE ( 'NONE', *, *, #8152, .T. ) ;
#10414=DIRECTION ( 'NONE',  ( -1.000000000000000078E-15, 1.000000000000000000, 0.000000000000000000 ) ) ;
#10432=CARTESIAN_POINT ( 'NONE',  ( -10.12832823130355209, -90.53875328855629334, -5.525617877236590481 ) ) ;
#10447=FACE_OUTER_BOUND ( 'NONE', #9693, .T. ) ;
#10512=CARTESIAN_POINT ( 'NONE',  ( -11.62590802060972628, -90.89463901465936146, -9.231817515786266526 ) ) ;
#10522=CARTESIAN_POINT ( 'NONE',  ( -20.87112600995945755, -109.5609729487397885, -2.351181146270280298 ) ) ;
#10600=EDGE_CURVE ( 'NONE', #14720, #1308, #3970, .T. ) ;
#10603=ORIENTED_EDGE ( 'NONE', *, *, #14237, .F. ) ;
#10631=CARTESIAN_POINT ( 'NONE',  ( -20.72181259498818306, -108.0168781946340033, -6.766942245938937894 ) ) ;
#10743=EDGE_CURVE ( 'NONE', #3090, #2245, #6541, .T. ) ;
#10763=ADVANCED_FACE ( 'NONE', ( #4263 ), #8994, .F. ) ;
#10765=DIRECTION ( 'NONE',  ( 1.000000000000000078E-15, -1.000000000000000000, 0.000000000000000000 ) ) ;
#10779=CARTESIAN_POINT ( 'NONE',  ( -10.12827371166239843, -85.00737899243800655, -5.497689735155993240 ) ) ;
#10798=FACE_OUTER_BOUND ( 'NONE', #11287, .T. ) ;
#10819=CARTESIAN_POINT ( 'NONE',  ( -10.74382054100576234, -90.63416536375187604, -7.998061603526264385 ) ) ;
#10847=CARTESIAN_POINT ( 'NONE',  ( -18.09969986081091875, -107.1622034095862972, -7.162689735156003934 ) ) ;
#10852=AXIS2_PLACEMENT_3D ( 'NONE', #1725, #10050, #2951 ) ;
#10860=CIRCLE ( 'NONE', #4758, 5.371426149148541107 ) ;
#10878=LINE ( 'NONE', #6486, #13127 ) ;
#10914=DIRECTION ( 'NONE',  ( 0.000000000000000000, 0.000000000000000000, -1.000000000000000000 ) ) ;
#10930=DIRECTION ( 'NONE',  ( 1.000000000000000000, 0.000000000000000000, 9.688619527525975741E-16 ) ) ;
#10965=CARTESIAN_POINT ( 'NONE',  ( -15.49969986081092976, -95.55504406891904523, -9.828641771674195837 ) ) ;
#10974=VERTEX_POINT ( 'NONE', #3238 ) ;
#10984=CARTESIAN_POINT ( 'NONE',  ( -20.63946442839013784, -106.6916975368905156, -7.058995725539832122 ) ) ;
#11009=CYLINDRICAL_SURFACE ( 'NONE', #2533, 5.371426149148541107 ) ;
#11095=AXIS2_PLACEMENT_3D ( 'NONE', #14731, #1180, #9285 ) ;
#11125=VERTEX_POINT ( 'NONE', #6581 ) ;
#11143=CARTESIAN_POINT ( 'NONE',  ( -18.09969986081091875, -107.1622034095862972, -6.087689735156002868 ) ) ;
#11209=B_SPLINE_CURVE_WITH_KNOTS ( 'NONE', 3,
 ( #1103, #5761, #10432, #15100, #6969, #4401, #9128, #9051, #7818, #12506, #5612, #3255, #12590, #11432, #959, #13807, #3324, #40, #10819, #4859, #3704, #1179, #7052, #10512, #1336, #269, #2410, #3552, #3854, #5908, #9437, #1486, #2559, #11729, #2705, #7129, #13203, #1252, #7208 ),
 .UNSPECIFIED., .F., .F.,
 ( 4, 2, 1, 1, 1, 2, 2, 2, 2, 1, 1, 1, 1, 2, 2, 2, 2, 1, 1, 1, 1, 2, 2, 2, 4 ),
 ( 0.5684180336906330400, 0.5701039007465288355, 0.5717897678024245200, 0.5751615019142162222, 0.5819049701377994044, 0.5953919065849659908, 0.6223657794792989417, 0.6763135252679648435, 0.6771564587959129078, 0.6779993923238609721, 0.6796852593797569897, 0.6830569934915491359, 0.6898004617151334283, 0.7032873981623020132, 0.7302612710566397380, 0.7842090168453148546, 0.7850519503732626969, 0.7858948839012106502, 0.7875807509571066678, 0.7909524850688987030, 0.7976959532924827734, 0.8111828897396505811, 0.8381567626339864185, 0.8921045084226580935, 1.000000000000000000 ),
 .UNSPECIFIED. ) ;
#11216=DIRECTION ( 'NONE',  ( -1.000000000000000078E-15, 1.000000000000000000, 0.000000000000000000 ) ) ;
#11262=ORIENTED_EDGE ( 'NONE', *, *, #10743, .F. ) ;
#11263=CARTESIAN_POINT ( 'NONE',  ( -20.87112600995945755, -109.7258744763782943, -5.497689735156006563 ) ) ;
#11287=EDGE_LOOP ( 'NONE', ( #3981, #11557 ) ) ;
#11359=DIRECTION ( 'NONE',  ( -1.000000000000000000, 0.000000000000000000, -1.011922027653137143E-15 ) ) ;
#11382=CARTESIAN_POINT ( 'NONE',  ( -11.44122778921134120, -90.82924336192752435, -1.978697273178005034 ) ) ;
#11432=CARTESIAN_POINT ( 'NONE',  ( -10.59381597806627795, -90.60492159835612824, -7.685054528635899551 ) ) ;
#11445=CARTESIAN_POINT ( 'NONE',  ( -15.97834026492444437, -93.97082955884093280, -10.96837812141254354 ) ) ;
#11458=CARTESIAN_POINT ( 'NONE',  ( -15.26264886222055139, -94.81047857984601990, -0.1311698051623074457 ) ) ;
#11533=CARTESIAN_POINT ( 'NONE',  ( -11.24943535381201087, -90.76549582974007535, -2.207202805067481677 ) ) ;
#11557=ORIENTED_EDGE ( 'NONE', *, *, #942, .F. ) ;
#11609=CARTESIAN_POINT ( 'NONE',  ( -15.44029880530547416, -95.51755032243795540, -0.1252850382680660568 ) ) ;
#11648=COLOUR_RGB ( '', 0.31764706, 0.68627451, 0.89019608) ;
#11729=CARTESIAN_POINT ( 'NONE',  ( -12.56680741991290340, -91.35574364345187348, -10.00076552370670768 ) ) ;
#11862=ORIENTED_EDGE ( 'NONE', *, *, #8152, .F. ) ;
#11878=VERTEX_POINT ( 'NONE', #5289 ) ;
#11917=FILL_AREA_STYLE ('',( #2155 ) ) ;
#11954=PRODUCT_DEFINITION_FORMATION_WITH_SPECIFIED_SOURCE ( 'ANY', '', #264, .NOT_KNOWN. ) ;
#11972=EDGE_CURVE ( 'NONE', #3521, #1308, #6721, .T. ) ;
#11998=( NAMED_UNIT ( * ) SI_UNIT ( $, .STERADIAN. ) SOLID_ANGLE_UNIT ( ) );
#12057=ORIENTED_EDGE ( 'NONE', *, *, #9107, .F. ) ;
#12125=ORIENTED_EDGE ( 'NONE', *, *, #2861, .T. ) ;
#12131=CARTESIAN_POINT ( 'NONE',  ( -20.82326471215695562, -106.0804592893369147, -6.239094581732940625 ) ) ;
#12155=CARTESIAN_POINT ( 'NONE',  ( -9.499699860810959962, -67.00737899243799234, -5.497689735155993240 ) ) ;
#12160=ORIENTED_EDGE ( 'NONE', *, *, #8847, .F. ) ;
#12225=CARTESIAN_POINT ( 'NONE',  ( -15.49969986081099904, -27.00737899243799944, -5.497689735156000346 ) ) ;
#12229=ADVANCED_FACE ( 'NONE', ( #4201 ), #11009, .T. ) ;
#12275=PLANE ( 'NONE',  #12414 ) ;
#12347=EDGE_LOOP ( 'NONE', ( #2699, #803, #9506, #12866, #14103, #14884, #2189, #7667, #6098, #3737 ) ) ;
#12414=AXIS2_PLACEMENT_3D ( 'NONE', #1867, #1637, #3010 ) ;
#12419=DIRECTION ( 'NONE',  ( 0.000000000000000000, 0.000000000000000000, 1.000000000000000000 ) ) ;
#12457=VECTOR ( 'NONE', #14818, 1000.000000000000114 ) ;
#12501=FACE_OUTER_BOUND ( 'NONE', #3393, .T. ) ;
#12506=CARTESIAN_POINT ( 'NONE',  ( -10.22659806069228416, -90.55000404333293318, -6.537620383987239769 ) ) ;
#12510=CARTESIAN_POINT ( 'NONE',  ( -10.12827371166237533, -110.0073789924380065, -5.497689735155995017 ) ) ;
#12515=VERTEX_POINT ( 'NONE', #8693 ) ;
#12520=CYLINDRICAL_SURFACE ( 'NONE', #2500, 1.074999999999999512 ) ;
#12537=CARTESIAN_POINT ( 'NONE',  ( -10.49759577181166215, -90.58864147777146059, -3.450279645307360976 ) ) ;
#12560=LINE ( 'NONE', #4525, #7607 ) ;
#12590=CARTESIAN_POINT ( 'NONE',  ( -10.59040657616195524, -90.60431240515791274, -7.677386969860795496 ) ) ;
#12591=AXIS2_PLACEMENT_3D ( 'NONE', #22, #10414, #1235 ) ;
#12603=DIRECTION ( 'NONE',  ( 1.000000000000000000, 1.000000000000000078E-15, 1.000000000000000078E-15 ) ) ;
#12615=CARTESIAN_POINT ( 'NONE',  ( -10.19698273680794820, -90.54727021874583670, -4.632518811245576629 ) ) ;
#12649=EDGE_CURVE ( 'NONE', #6778, #2175, #7035, .T. ) ;
#12690=CARTESIAN_POINT ( 'NONE',  ( -13.28192010678624868, -91.85033406443031367, -0.6052620916867849088 ) ) ;
#12714=CARTESIAN_POINT ( 'NONE',  ( -21.49969986081095996, -67.00737899243799234, -5.497689735156007451 ) ) ;
#12771=CARTESIAN_POINT ( 'NONE',  ( -10.22863128988245229, -90.55140526738702533, -4.451800774622809875 ) ) ;
#12790=CARTESIAN_POINT ( 'NONE',  ( -20.60655739512267104, -107.3584631001859719, -7.162689735156004822 ) ) ;
#12848=CARTESIAN_POINT ( 'NONE',  ( -10.27578761138057040, -90.55771581991869823, -4.244953887782999757 ) ) ;
#12856=CARTESIAN_POINT ( 'NONE',  ( -18.09969986081091164, -110.0073789924380065, -10.19792577984107318 ) ) ;
#12866=ORIENTED_EDGE ( 'NONE', *, *, #14766, .F. ) ;
#12877=( NAMED_UNIT ( * ) SI_UNIT ( $, .STERADIAN. ) SOLID_ANGLE_UNIT ( ) );
#12892=AXIS2_PLACEMENT_3D ( 'NONE', #1509, #13225, #8541 ) ;
#12921=LINE ( 'NONE', #60, #3568 ) ;
#12944=CARTESIAN_POINT ( 'NONE',  ( -20.68303597405226313, -107.8803405083532567, -6.910450545281812573 ) ) ;
#12992=ADVANCED_FACE ( 'NONE', ( #4844 ), #14093, .T. ) ;
#13074=EDGE_LOOP ( 'NONE', ( #974, #8603, #5112, #14098, #2828 ) ) ;
#13076=PRESENTATION_STYLE_ASSIGNMENT (( #8622 ) ) ;
#13107=SHAPE_REPRESENTATION_RELATIONSHIP ( 'NONE' , 'NONE' ,  #2852, #76 ) ;
#13127=VECTOR ( 'NONE', #1687, 1000.000000000000114 ) ;
#13155=( NAMED_UNIT ( * ) PLANE_ANGLE_UNIT ( ) SI_UNIT ( $, .RADIAN. ) );
#13203=CARTESIAN_POINT ( 'NONE',  ( -14.04486373469046434, -92.52292627908343547, -10.69836684062160437 ) ) ;
#13204=APPLICATION_CONTEXT ( 'automotive_design' ) ;
#13225=DIRECTION ( 'NONE',  ( 1.000000000000000078E-15, -1.000000000000000000, 0.000000000000000000 ) ) ;
#13386=DIRECTION ( 'NONE',  ( -1.000000000000000078E-15, 1.000000000000000000, 0.000000000000000000 ) ) ;
#13472=DIRECTION ( 'NONE',  ( -1.000000000000000078E-15, 0.000000000000000000, 1.000000000000000000 ) ) ;
#13538=DIRECTION ( 'NONE',  ( 1.000000000000000000, 0.000000000000000000, 9.688619527525975741E-16 ) ) ;
#13571=EDGE_CURVE ( 'NONE', #2017, #14153, #6529, .T. ) ;
#13601=DIRECTION ( 'NONE',  ( 0.000000000000000000, 0.000000000000000000, -1.000000000000000000 ) ) ;
#13611=STYLED_ITEM ( 'NONE', ( #13076 ), #2616 ) ;
#13638=CIRCLE ( 'NONE', #3625, 5.371426149148541107 ) ;
#13648=DIRECTION ( 'NONE',  ( -1.000000000000000078E-15, 1.000000000000000000, 0.000000000000000000 ) ) ;
#13675=CARTESIAN_POINT ( 'NONE',  ( -100.5053766806731090, -107.1622034095863825, -6.087689735156085469 ) ) ;
#13684=CARTESIAN_POINT ( 'NONE',  ( -14.93044674059276034, -93.95605536819624604, -0.1564500571729600387 ) ) ;
#13712=VECTOR ( 'NONE', #6763, 1000.000000000000000 ) ;
#13757=CARTESIAN_POINT ( 'NONE',  ( -11.40937861856655999, -90.81835191606845115, -2.015739043402887898 ) ) ;
#13798=ORIENTED_EDGE ( 'NONE', *, *, #1720, .T. ) ;
#13807=CARTESIAN_POINT ( 'NONE',  ( -10.60715604080722940, -90.60733076827288812, -7.714789323137090093 ) ) ;
#13813=ORIENTED_EDGE ( 'NONE', *, *, #11972, .F. ) ;
#13827=EDGE_CURVE ( 'NONE', #10974, #5139, #14687, .T. ) ;
#13830=CARTESIAN_POINT ( 'NONE',  ( -14.26921869364951867, -92.83203452458182880, -0.2586353043396797391 ) ) ;
#13833=LINE ( 'NONE', #13983, #2133 ) ;
#13834=DIRECTION ( 'NONE',  ( 0.000000000000000000, 0.000000000000000000, -1.000000000000000000 ) ) ;
#13843=CARTESIAN_POINT ( 'NONE',  ( -18.09969986081092230, -100.8057294739168839, -7.021413858388602769 ) ) ;
#13862=CARTESIAN_POINT ( 'NONE',  ( -20.86957454690095304, -106.3702754883801873, -5.355332227506997000 ) ) ;
#13938=EDGE_CURVE ( 'NONE', #3375, #6778, #4515, .T. ) ;
#13980=CARTESIAN_POINT ( 'NONE',  ( -13.15284510314214295, -91.74749311801966201, -0.6644210899480663679 ) ) ;
#13983=CARTESIAN_POINT ( 'NONE',  ( -9.499699860810959962, -67.00737899243799234, -5.497689735155993240 ) ) ;
#14008=ORIENTED_EDGE ( 'NONE', *, *, #14237, .T. ) ;
#14082=ORIENTED_EDGE ( 'NONE', *, *, #9952, .T. ) ;
#14093=CYLINDRICAL_SURFACE ( 'NONE', #2064, 5.371426149148541107 ) ;
#14098=ORIENTED_EDGE ( 'NONE', *, *, #749, .F. ) ;
#14103=ORIENTED_EDGE ( 'NONE', *, *, #2030, .T. ) ;
#14109=EDGE_CURVE ( 'NONE', #9733, #3638, #228, .T. ) ;
#14117=ORIENTED_EDGE ( 'NONE', *, *, #3326, .T. ) ;
#14133=B_SPLINE_CURVE_WITH_KNOTS ( 'NONE', 3,
 ( #8609, #583, #2801, #12131, #2949, #5246, #6305, #10984, #6523, #5165, #9838, #14505 ),
 .UNSPECIFIED., .F., .F.,
 ( 4, 2, 2, 2, 2, 4 ),
 ( 0.004466813839283045873, 0.005050776363214819209, 0.005634738887146591678, 0.006218701411078365014, 0.006510682673044269030, 0.006802663935010173045 ),
 .UNSPECIFIED. ) ;
#14153=VERTEX_POINT ( 'NONE', #10779 ) ;
#14237=EDGE_CURVE ( 'NONE', #6582, #3521, #8698, .T. ) ;
#14357=( GEOMETRIC_REPRESENTATION_CONTEXT ( 3 ) GLOBAL_UNCERTAINTY_ASSIGNED_CONTEXT ( ( #8755 ) ) GLOBAL_UNIT_ASSIGNED_CONTEXT ( ( #7393, #13155, #11998 ) ) REPRESENTATION_CONTEXT ( 'NONE', 'WORKASPACE' ) );
#14391=CARTESIAN_POINT ( 'NONE',  ( -20.87112600995945755, -108.0608273576312968, -5.497689735156002122 ) ) ;
#14462=CARTESIAN_POINT ( 'NONE',  ( -15.49969986081093509, -96.50737899243799234, -0.1262635860074601546 ) ) ;
#14474=DIRECTION ( 'NONE',  ( 1.000000000000000000, 0.000000000000000000, 1.011922027653137537E-15 ) ) ;
#14504=VECTOR ( 'NONE', #9209, 1000.000000000000000 ) ;
#14505=CARTESIAN_POINT ( 'NONE',  ( -20.60655739512266749, -107.1622034095862972, -7.162689735156005710 ) ) ;
#14603=ORIENTED_EDGE ( 'NONE', *, *, #1101, .F. ) ;
#14687=LINE ( 'NONE', #3054, #9341 ) ;
#14703=ORIENTED_EDGE ( 'NONE', *, *, #8932, .T. ) ;
#14720=VERTEX_POINT ( 'NONE', #3094 ) ;
#14731=CARTESIAN_POINT ( 'NONE',  ( -15.49969986081099904, -27.00737899243799944, -5.497689735156000346 ) ) ;
#14739=VECTOR ( 'NONE', #8181, 1000.000000000000000 ) ;
#14742=CARTESIAN_POINT ( 'NONE',  ( -17.09996058126371565, -94.70595027845364200, -10.75094526697130703 ) ) ;
#14766=EDGE_CURVE ( 'NONE', #2942, #10974, #14133, .T. ) ;
#14798=DIRECTION ( 'NONE',  ( 1.050965490997518184E-15, -0.05233595624294409832, -0.9986295347545739443 ) ) ;
#14800=CARTESIAN_POINT ( 'NONE',  ( -15.49969986081095996, -67.00737899243799234, -5.497689735156000346 ) ) ;
#14818=DIRECTION ( 'NONE',  ( -0.03489949670250103858, 0.9993908270190956511, -3.489949670250003432E-17 ) ) ;
#14824=ORIENTED_EDGE ( 'NONE', *, *, #7827, .F. ) ;
#14825=CARTESIAN_POINT ( 'NONE',  ( -15.05574454978227550, -94.23694090986742822, -0.1444574119560445569 ) ) ;
#14840=CARTESIAN_POINT ( 'NONE',  ( -15.49969986081092266, -107.6986194064928100, -1.942511738887820361 ) ) ;
#14858=CARTESIAN_POINT ( 'NONE',  ( -20.87112600995946821, -106.3120414409460466, -5.423877709286933246 ) ) ;
#14873=EDGE_CURVE ( 'NONE', #8778, #3521, #5339, .T. ) ;
#14884=ORIENTED_EDGE ( 'NONE', *, *, #1101, .T. ) ;
#14899=EDGE_CURVE ( 'NONE', #2017, #2175, #11209, .T. ) ;
#15008=CARTESIAN_POINT ( 'NONE',  ( -20.85369739404940148, -106.8082859091853862, -5.057075470912998583 ) ) ;
#15048=CARTESIAN_POINT ( 'NONE',  ( -13.02077215656149889, -91.65099479865030219, -0.7314108185287553354 ) ) ;
#15067=CARTESIAN_POINT ( 'NONE',  ( -20.60655739512266749, -107.1622034095862972, -7.162689735156005710 ) ) ;
#15089=ORIENTED_EDGE ( 'NONE', *, *, #8847, .T. ) ;
#15100=CARTESIAN_POINT ( 'NONE',  ( -10.12854551587539298, -90.53879060557073899, -5.553494450699679064 ) ) ;
ENDSEC;
END-ISO-10303-21;
